ISO-10303-21;
HEADER;
/* Generated by software containing ST-Developer
 * from STEP Tools, Inc. (www.steptools.com) 
 */

FILE_DESCRIPTION(
/* description */ ('PAT-015'),
/* implementation_level */ '2;1');

FILE_NAME(
/* name */ 'Flat Washer - M8.step',
/* time_stamp */ '2026-10-29T16:03:43-07:00',
/* author */ (''),
/* organization */ (''),
/* preprocessor_version */ 'ST-DEVELOPER v20.2',
/* originating_system */ 'Autodesk Translation Framework v15.17.0.0',
/* authorisation */ '');

FILE_SCHEMA (('AUTOMOTIVE_DESIGN { 1 0 10303 214 3 1 1 }'));
ENDSEC;

DATA;
#10=MECHANICAL_DESIGN_GEOMETRIC_PRESENTATION_REPRESENTATION('',(#249),#10266);
#201=SHAPE_REPRESENTATION_RELATIONSHIP('SRR','None',#10372,#224);
#224=ADVANCED_BREP_SHAPE_REPRESENTATION('',(#273),#10260);
#249=STYLED_ITEM('',(#10554),#273);
#273=MANIFOLD_SOLID_BREP('Body1',#4709);
#412=FACE_BOUND('',#1208,.T.);
#413=FACE_BOUND('',#1210,.T.);
#535=PLANE('',#5446);
#536=PLANE('',#5447);
#802=FACE_OUTER_BOUND('',#1205,.T.);
#803=FACE_OUTER_BOUND('',#1206,.T.);
#804=FACE_OUTER_BOUND('',#1207,.T.);
#805=FACE_OUTER_BOUND('',#1209,.T.);
#1205=EDGE_LOOP('',(#4081,#4082,#4083,#4084));
#1206=EDGE_LOOP('',(#4085,#4086,#4087,#4088));
#1207=EDGE_LOOP('',(#4089));
#1208=EDGE_LOOP('',(#4090));
#1209=EDGE_LOOP('',(#4091));
#1210=EDGE_LOOP('',(#4092));
#1534=LINE('',#9933,#1814);
#1535=LINE('',#9939,#1815);
#1814=VECTOR('',#6711,0.42);
#1815=VECTOR('',#6718,0.8);
#2090=CIRCLE('',#5441,0.42);
#2091=CIRCLE('',#5442,0.42);
#2092=CIRCLE('',#5444,0.8);
#2093=CIRCLE('',#5445,0.8);
#2439=VERTEX_POINT('',#9930);
#2440=VERTEX_POINT('',#9932);
#2441=VERTEX_POINT('',#9936);
#2442=VERTEX_POINT('',#9938);
#2996=EDGE_CURVE('',#2439,#2439,#2090,.T.);
#2997=EDGE_CURVE('',#2439,#2440,#1534,.T.);
#2998=EDGE_CURVE('',#2440,#2440,#2091,.T.);
#2999=EDGE_CURVE('',#2441,#2441,#2092,.T.);
#3000=EDGE_CURVE('',#2441,#2442,#1535,.T.);
#3001=EDGE_CURVE('',#2442,#2442,#2093,.T.);
#4081=ORIENTED_EDGE('',*,*,#2996,.F.);
#4082=ORIENTED_EDGE('',*,*,#2997,.T.);
#4083=ORIENTED_EDGE('',*,*,#2998,.T.);
#4084=ORIENTED_EDGE('',*,*,#2997,.F.);
#4085=ORIENTED_EDGE('',*,*,#2999,.F.);
#4086=ORIENTED_EDGE('',*,*,#3000,.T.);
#4087=ORIENTED_EDGE('',*,*,#3001,.T.);
#4088=ORIENTED_EDGE('',*,*,#3000,.F.);
#4089=ORIENTED_EDGE('',*,*,#2999,.T.);
#4090=ORIENTED_EDGE('',*,*,#2996,.T.);
#4091=ORIENTED_EDGE('',*,*,#3001,.F.);
#4092=ORIENTED_EDGE('',*,*,#2998,.F.);
#4399=CYLINDRICAL_SURFACE('',#5440,0.42);
#4400=CYLINDRICAL_SURFACE('',#5443,0.8);
#4637=ADVANCED_FACE('',(#802),#4399,.F.);
#4638=ADVANCED_FACE('',(#803),#4400,.T.);
#4639=ADVANCED_FACE('',(#804,#412),#535,.T.);
#4640=ADVANCED_FACE('',(#805,#413),#536,.F.);
#4709=CLOSED_SHELL('',(#4637,#4638,#4639,#4640));
#5439=AXIS2_PLACEMENT_3D('',#9928,#6705,#6706);
#5440=AXIS2_PLACEMENT_3D('',#9929,#6707,#6708);
#5441=AXIS2_PLACEMENT_3D('',#9931,#6709,#6710);
#5442=AXIS2_PLACEMENT_3D('',#9934,#6712,#6713);
#5443=AXIS2_PLACEMENT_3D('',#9935,#6714,#6715);
#5444=AXIS2_PLACEMENT_3D('',#9937,#6716,#6717);
#5445=AXIS2_PLACEMENT_3D('',#9940,#6719,#6720);
#5446=AXIS2_PLACEMENT_3D('',#9941,#6721,#6722);
#5447=AXIS2_PLACEMENT_3D('',#9942,#6723,#6724);
#6705=DIRECTION('axis',(0.,0.,1.));
#6706=DIRECTION('refdir',(1.,0.,0.));
#6707=DIRECTION('center_axis',(0.,1.,0.));
#6708=DIRECTION('ref_axis',(1.,0.,0.));
#6709=DIRECTION('center_axis',(0.,-1.,0.));
#6710=DIRECTION('ref_axis',(1.,0.,0.));
#6711=DIRECTION('',(0.,-1.,0.));
#6712=DIRECTION('center_axis',(0.,-1.,0.));
#6713=DIRECTION('ref_axis',(1.,0.,0.));
#6714=DIRECTION('center_axis',(0.,1.,0.));
#6715=DIRECTION('ref_axis',(1.,0.,0.));
#6716=DIRECTION('center_axis',(0.,1.,0.));
#6717=DIRECTION('ref_axis',(1.,0.,0.));
#6718=DIRECTION('',(0.,-1.,0.));
#6719=DIRECTION('center_axis',(0.,1.,0.));
#6720=DIRECTION('ref_axis',(1.,0.,0.));
#6721=DIRECTION('center_axis',(0.,1.,0.));
#6722=DIRECTION('ref_axis',(1.,0.,0.));
#6723=DIRECTION('center_axis',(0.,1.,0.));
#6724=DIRECTION('ref_axis',(1.,0.,0.));
#9928=CARTESIAN_POINT('',(0.,0.,0.));
#9929=CARTESIAN_POINT('Origin',(0.,0.,0.));
#9930=CARTESIAN_POINT('',(-0.42,0.16,5.14351655641888E-17));
#9931=CARTESIAN_POINT('Origin',(0.,0.16,0.));
#9932=CARTESIAN_POINT('',(-0.42,0.,5.14351655641888E-17));
#9933=CARTESIAN_POINT('',(-0.42,0.,5.14351655641888E-17));
#9934=CARTESIAN_POINT('Origin',(0.,0.,0.));
#9935=CARTESIAN_POINT('Origin',(0.,0.,0.));
#9936=CARTESIAN_POINT('',(-0.8,0.16,9.79717439317883E-17));
#9937=CARTESIAN_POINT('Origin',(0.,0.16,0.));
#9938=CARTESIAN_POINT('',(-0.8,0.,9.79717439317883E-17));
#9939=CARTESIAN_POINT('',(-0.8,0.,9.79717439317883E-17));
#9940=CARTESIAN_POINT('Origin',(0.,0.,0.));
#9941=CARTESIAN_POINT('Origin',(0.,0.16,0.));
#9942=CARTESIAN_POINT('Origin',(0.,0.,0.));
#10235=UNCERTAINTY_MEASURE_WITH_UNIT(LENGTH_MEASURE(0.001),#10267,
'DISTANCE_ACCURACY_VALUE',
'Maximum model space distance between geometric entities at asserted c
onnectivities');
#10241=UNCERTAINTY_MEASURE_WITH_UNIT(LENGTH_MEASURE(0.001),#10267,
'DISTANCE_ACCURACY_VALUE',
'Maximum model space distance between geometric entities at asserted c
onnectivities');
#10260=(
GEOMETRIC_REPRESENTATION_CONTEXT(3)
GLOBAL_UNCERTAINTY_ASSIGNED_CONTEXT((#10235))
GLOBAL_UNIT_ASSIGNED_CONTEXT((#10267,#10269,#10270))
REPRESENTATION_CONTEXT('','3D')
);
#10266=(
GEOMETRIC_REPRESENTATION_CONTEXT(3)
GLOBAL_UNCERTAINTY_ASSIGNED_CONTEXT((#10241))
GLOBAL_UNIT_ASSIGNED_CONTEXT((#10267,#10269,#10270))
REPRESENTATION_CONTEXT('','3D')
);
#10267=(
LENGTH_UNIT()
NAMED_UNIT(*)
SI_UNIT(.CENTI.,.METRE.)
);
#10269=(
NAMED_UNIT(*)
PLANE_ANGLE_UNIT()
SI_UNIT($,.RADIAN.)
);
#10270=(
NAMED_UNIT(*)
SI_UNIT($,.STERADIAN.)
SOLID_ANGLE_UNIT()
);
#10289=SHAPE_DEFINITION_REPRESENTATION(#10313,#10372);
#10313=PRODUCT_DEFINITION_SHAPE('',$,#10397);
#10372=SHAPE_REPRESENTATION('',(#5439),#10260);
#10378=PRODUCT_DEFINITION_CONTEXT('part definition',#10452,'design');
#10397=PRODUCT_DEFINITION('Flat Washer - M8','Flat Washer - M8',
#10421,#10378);
#10421=PRODUCT_DEFINITION_FORMATION('',$,#10472);
#10452=APPLICATION_CONTEXT(
'Core Data for Automotive Mechanical Design Process');
#10453=PRODUCT_CONTEXT('part definition',#10452,'mechanical');
#10472=PRODUCT('Flat Washer - M8','Flat Washer - M8',
'Flat Washer - M8',(#10453));
#10548=COLOUR_RGB('Black',0.12,0.14,0.17);
#10549=FILL_AREA_STYLE_COLOUR('',#10548);
#10550=FILL_AREA_STYLE('',(#10549));
#10551=SURFACE_STYLE_FILL_AREA(#10550);
#10552=SURFACE_SIDE_STYLE('',(#10551));
#10553=SURFACE_STYLE_USAGE(.BOTH.,#10552);
#10554=PRESENTATION_STYLE_ASSIGNMENT((#10553));
ENDSEC;
END-ISO-10303-21;
